ISO-10303-21;
HEADER;
FILE_DESCRIPTION (('STEP AP214'),
    '1' );
FILE_NAME ('Part3.step',
    '2026-11-01T05:08:46',
    ( '' ),
    ( '' ),
    'SwSTEP 2.0',
    'SolidWorks 2024',
    '' );
FILE_SCHEMA (( 'AUTOMOTIVE_DESIGN' ));
ENDSEC;

DATA;
#194=EDGE_CURVE ( 'NONE', #1410, #15340, #14768, .T. ) ;
#198=LINE ( 'NONE', #13428, #14938 ) ;
#317=LINE ( 'NONE', #2711, #1003 ) ;
#332=DIRECTION ( 'NONE',  ( 0.000000000000000000, -1.000000000000000000, 0.000000000000000000 ) ) ;
#385=DIRECTION ( 'NONE',  ( 1.000000000000000000, -0.000000000000000000, -0.000000000000000000 ) ) ;
#414=VERTEX_POINT ( 'NONE', #2628 ) ;
#422=LINE ( 'NONE', #9526, #6191 ) ;
#428=DIRECTION ( 'NONE',  ( -0.000000000000000000, -0.000000000000000000, 1.000000000000000000 ) ) ;
#527=DIRECTION ( 'NONE',  ( 1.000000000000000000, 0.000000000000000000, 0.000000000000000000 ) ) ;
#532=ORIENTED_EDGE ( 'NONE', *, *, #12548, .F. ) ;
#545=PLANE ( 'NONE',  #2000 ) ;
#561=VECTOR ( 'NONE', #5113, 1000.000000000000000 ) ;
#578=LINE ( 'NONE', #3243, #14140 ) ;
#616=ORIENTED_EDGE ( 'NONE', *, *, #4791, .F. ) ;
#690=ORIENTED_EDGE ( 'NONE', *, *, #1012, .F. ) ;
#709=SHAPE_DEFINITION_REPRESENTATION ( #16201, #16471 ) ;
#898=ADVANCED_FACE ( 'NONE', ( #9051 ), #14288, .F. ) ;
#906=CARTESIAN_POINT ( 'NONE',  ( -270.0000000000000000, 0.000000000000000000, 0.000000000000000000 ) ) ;
#920=ADVANCED_FACE ( 'NONE', ( #10597 ), #4151, .F. ) ;
#1003=VECTOR ( 'NONE', #9329, 1000.000000000000000 ) ;
#1012=EDGE_CURVE ( 'NONE', #2613, #16499, #12145, .T. ) ;
#1023=ADVANCED_FACE ( 'NONE', ( #2223 ), #1910, .T. ) ;
#1034=DIRECTION ( 'NONE',  ( -0.000000000000000000, 1.000000000000000000, -0.000000000000000000 ) ) ;
#1035=PLANE ( 'NONE',  #1461 ) ;
#1069=VERTEX_POINT ( 'NONE', #1840 ) ;
#1109=ADVANCED_FACE ( 'NONE', ( #10942 ), #1035, .T. ) ;
#1141=DIRECTION ( 'NONE',  ( 0.000000000000000000, -1.000000000000000000, 0.000000000000000000 ) ) ;
#1168=APPLICATION_CONTEXT ( 'automotive_design' ) ;
#1174=ORIENTED_EDGE ( 'NONE', *, *, #8965, .F. ) ;
#1178=AXIS2_PLACEMENT_3D ( 'NONE', #16090, #14727, #5434 ) ;
#1291=LINE ( 'NONE', #10728, #11364 ) ;
#1320=DIRECTION ( 'NONE',  ( 0.000000000000000000, 1.000000000000000000, 0.000000000000000000 ) ) ;
#1342=EDGE_CURVE ( 'NONE', #7123, #3171, #5567, .T. ) ;
#1349=DIRECTION ( 'NONE',  ( -0.000000000000000000, -0.000000000000000000, 1.000000000000000000 ) ) ;
#1359=DIRECTION ( 'NONE',  ( 1.000000000000000000, -0.000000000000000000, -0.000000000000000000 ) ) ;
#1367=VECTOR ( 'NONE', #2102, 1000.000000000000000 ) ;
#1410=VERTEX_POINT ( 'NONE', #9065 ) ;
#1458=CARTESIAN_POINT ( 'NONE',  ( -270.0000000000000000, 512.1906115401388888, -11.00000000000000000 ) ) ;
#1461=AXIS2_PLACEMENT_3D ( 'NONE', #8764, #11423, #14176 ) ;
#1466=EDGE_LOOP ( 'NONE', ( #7727, #15131, #2330, #10352, #8900, #4321 ) ) ;
#1472=CARTESIAN_POINT ( 'NONE',  ( -440.0000000000000568, 425.7506394335853201, -11.00000000000000000 ) ) ;
#1473=EDGE_LOOP ( 'NONE', ( #2266, #6265, #690, #7755, #616, #13974 ) ) ;
#1488=AXIS2_PLACEMENT_3D ( 'NONE', #3280, #8693, #15217 ) ;
#1496=VERTEX_POINT ( 'NONE', #10362 ) ;
#1504=PRODUCT_DEFINITION_FORMATION_WITH_SPECIFIED_SOURCE ( 'ANY', '', #2165, .NOT_KNOWN. ) ;
#1642=FILL_AREA_STYLE_COLOUR ( '', #5591 ) ;
#1652=EDGE_CURVE ( 'NONE', #7313, #10036, #5533, .T. ) ;
#1788=CARTESIAN_POINT ( 'NONE',  ( -210.0000000000000000, 512.1906115401388888, 0.000000000000000000 ) ) ;
#1816=ORIENTED_EDGE ( 'NONE', *, *, #8125, .T. ) ;
#1840=CARTESIAN_POINT ( 'NONE',  ( 0.000000000000000000, 425.7506394335853201, 109.9999999999999858 ) ) ;
#1910=PLANE ( 'NONE',  #12161 ) ;
#1964=VERTEX_POINT ( 'NONE', #7035 ) ;
#1965=LINE ( 'NONE', #7280, #12674 ) ;
#1999=ORIENTED_EDGE ( 'NONE', *, *, #8965, .T. ) ;
#2000=AXIS2_PLACEMENT_3D ( 'NONE', #13436, #6879, #12137 ) ;
#2012=LINE ( 'NONE', #16190, #16374 ) ;
#2040=DIRECTION ( 'NONE',  ( -1.000000000000000000, 0.000000000000000000, -0.000000000000000000 ) ) ;
#2049=EDGE_CURVE ( 'NONE', #1069, #9318, #15108, .T. ) ;
#2067=DIRECTION ( 'NONE',  ( -0.000000000000000000, 1.000000000000000000, -0.000000000000000000 ) ) ;
#2102=DIRECTION ( 'NONE',  ( 0.000000000000000000, 1.000000000000000000, 0.000000000000000000 ) ) ;
#2165=PRODUCT ( 'Part3', 'Part3', '', ( #7454 ) ) ;
#2210=DIRECTION ( 'NONE',  ( -0.000000000000000000, 0.000000000000000000, -1.000000000000000000 ) ) ;
#2223=FACE_OUTER_BOUND ( 'NONE', #4703, .T. ) ;
#2237=VECTOR ( 'NONE', #1349, 1000.000000000000000 ) ;
#2253=VECTOR ( 'NONE', #8755, 1000.000000000000000 ) ;
#2266=ORIENTED_EDGE ( 'NONE', *, *, #5198, .T. ) ;
#2285=ORIENTED_EDGE ( 'NONE', *, *, #13399, .F. ) ;
#2301=VECTOR ( 'NONE', #16413, 1000.000000000000000 ) ;
#2330=ORIENTED_EDGE ( 'NONE', *, *, #10754, .T. ) ;
#2337=ORIENTED_EDGE ( 'NONE', *, *, #1652, .T. ) ;
#2405=ORIENTED_EDGE ( 'NONE', *, *, #1012, .T. ) ;
#2421=CARTESIAN_POINT ( 'NONE',  ( 10.00000000000000000, 620.7506394335853201, -11.00000000000000000 ) ) ;
#2484=DIRECTION ( 'NONE',  ( 1.000000000000000000, 0.000000000000000000, 0.000000000000000000 ) ) ;
#2514=AXIS2_PLACEMENT_3D ( 'NONE', #12437, #3422, #14939 ) ;
#2539=CARTESIAN_POINT ( 'NONE',  ( -150.0000000000000284, 620.7506394335853201, 0.000000000000000000 ) ) ;
#2594=CARTESIAN_POINT ( 'NONE',  ( 10.00000000000000000, 425.7506394335853201, 0.000000000000000000 ) ) ;
#2611=LINE ( 'NONE', #7837, #7043 ) ;
#2613=VERTEX_POINT ( 'NONE', #7835 ) ;
#2628=CARTESIAN_POINT ( 'NONE',  ( 10.00000000000000000, 620.7506394335853201, 109.9999999999999858 ) ) ;
#2643=CARTESIAN_POINT ( 'NONE',  ( 10.00000000000000000, 620.7506394335853201, -11.00000000000000000 ) ) ;
#2666=ORIENTED_EDGE ( 'NONE', *, *, #11273, .F. ) ;
#2671=VECTOR ( 'NONE', #1034, 1000.000000000000000 ) ;
#2711=CARTESIAN_POINT ( 'NONE',  ( 10.00000000000000000, 620.7506394335853201, -11.00000000000000000 ) ) ;
#2767=LINE ( 'NONE', #12906, #15992 ) ;
#2780=VECTOR ( 'NONE', #428, 1000.000000000000000 ) ;
#2803=AXIS2_PLACEMENT_3D ( 'NONE', #14261, #2484, #14515 ) ;
#2853=ORIENTED_EDGE ( 'NONE', *, *, #8241, .F. ) ;
#2948=FACE_OUTER_BOUND ( 'NONE', #4906, .T. ) ;
#3006=MANIFOLD_SOLID_BREP ( 'Boss-Extrude4', #16496 ) ;
#3036=APPLICATION_CONTEXT ( 'automotive_design' ) ;
#3047=VERTEX_POINT ( 'NONE', #1472 ) ;
#3123=CARTESIAN_POINT ( 'NONE',  ( -150.0000000000000284, 620.7506394335853201, -11.00000000000000000 ) ) ;
#3171=VERTEX_POINT ( 'NONE', #3779 ) ;
#3243=CARTESIAN_POINT ( 'NONE',  ( 10.00000000000000000, 620.7506394335853201, 109.9999999999999858 ) ) ;
#3280=CARTESIAN_POINT ( 'NONE',  ( 0.000000000000000000, 0.000000000000000000, 0.000000000000000000 ) ) ;
#3349=CARTESIAN_POINT ( 'NONE',  ( 10.00000000000000000, 620.7506394335853201, -11.00000000000000000 ) ) ;
#3405=DIRECTION ( 'NONE',  ( 1.000000000000000000, -0.000000000000000000, -0.000000000000000000 ) ) ;
#3422=DIRECTION ( 'NONE',  ( -0.000000000000000000, 0.000000000000000000, 1.000000000000000000 ) ) ;
#3425=ADVANCED_FACE ( 'NONE', ( #13895 ), #13732, .T. ) ;
#3444=LINE ( 'NONE', #11422, #2671 ) ;
#3496=DIRECTION ( 'NONE',  ( -1.000000000000000000, 0.000000000000000000, 0.000000000000000000 ) ) ;
#3512=AXIS2_PLACEMENT_3D ( 'NONE', #8664, #2040, #13896 ) ;
#3567=DIRECTION ( 'NONE',  ( 1.000000000000000000, 0.000000000000000000, 0.000000000000000000 ) ) ;
#3681=AXIS2_PLACEMENT_3D ( 'NONE', #5046, #10461, #3775 ) ;
#3722=VERTEX_POINT ( 'NONE', #2539 ) ;
#3728=LINE ( 'NONE', #6272, #5030 ) ;
#3741=ORIENTED_EDGE ( 'NONE', *, *, #9634, .T. ) ;
#3743=AXIS2_PLACEMENT_3D ( 'NONE', #3349, #8424, #8675 ) ;
#3775=DIRECTION ( 'NONE',  ( 1.000000000000000000, 0.000000000000000000, 0.000000000000000000 ) ) ;
#3779=CARTESIAN_POINT ( 'NONE',  ( 0.000000000000000000, 620.7506394335853201, 0.000000000000000000 ) ) ;
#3807=DIRECTION ( 'NONE',  ( -1.000000000000000000, 0.000000000000000000, -0.000000000000000000 ) ) ;
#3896=CARTESIAN_POINT ( 'NONE',  ( -440.0000000000000568, 425.7506394335853201, 109.9999999999999858 ) ) ;
#4037=EDGE_CURVE ( 'NONE', #13742, #10036, #6267, .T. ) ;
#4064=EDGE_CURVE ( 'NONE', #13088, #11305, #198, .T. ) ;
#4151=PLANE ( 'NONE',  #1178 ) ;
#4207=VECTOR ( 'NONE', #16518, 1000.000000000000000 ) ;
#4222=SURFACE_SIDE_STYLE ('',( #13241 ) ) ;
#4256=EDGE_CURVE ( 'NONE', #3047, #2613, #5759, .T. ) ;
#4266=DIRECTION ( 'NONE',  ( -0.000000000000000000, -0.000000000000000000, -1.000000000000000000 ) ) ;
#4321=ORIENTED_EDGE ( 'NONE', *, *, #7702, .F. ) ;
#4363=LINE ( 'NONE', #9928, #10849 ) ;
#4420=EDGE_LOOP ( 'NONE', ( #14868, #13648, #5990, #4601, #12019, #15245, #8016, #2666 ) ) ;
#4432=DIRECTION ( 'NONE',  ( 0.000000000000000000, -1.000000000000000000, 0.000000000000000000 ) ) ;
#4601=ORIENTED_EDGE ( 'NONE', *, *, #4037, .T. ) ;
#4703=EDGE_LOOP ( 'NONE', ( #12505, #12097, #12154, #4953, #14764, #2405, #16340, #11690 ) ) ;
#4734=VECTOR ( 'NONE', #385, 1000.000000000000000 ) ;
#4751=DIRECTION ( 'NONE',  ( 2.556703065963791256E-16, -1.000000000000000000, 0.000000000000000000 ) ) ;
#4791=EDGE_CURVE ( 'NONE', #8452, #11485, #11403, .T. ) ;
#4825=ORIENTED_EDGE ( 'NONE', *, *, #15868, .F. ) ;
#4847=DIRECTION ( 'NONE',  ( 0.000000000000000000, -0.000000000000000000, 1.000000000000000000 ) ) ;
#4873=CARTESIAN_POINT ( 'NONE',  ( 0.000000000000000000, 620.7506394335853201, 305.2562418976663707 ) ) ;
#4886=EDGE_CURVE ( 'NONE', #14448, #9650, #6482, .T. ) ;
#4891=CARTESIAN_POINT ( 'NONE',  ( 0.000000000000000000, 0.000000000000000000, -11.00000000000000000 ) ) ;
#4906=EDGE_LOOP ( 'NONE', ( #10943, #4825, #8516, #2285 ) ) ;
#4946=EDGE_LOOP ( 'NONE', ( #11020, #16073, #15657, #2337 ) ) ;
#4953=ORIENTED_EDGE ( 'NONE', *, *, #11273, .T. ) ;
#4959=LINE ( 'NONE', #15453, #12783 ) ;
#5022=CARTESIAN_POINT ( 'NONE',  ( -270.0000000000000000, 620.7506394335853201, -11.00000000000000000 ) ) ;
#5030=VECTOR ( 'NONE', #1141, 1000.000000000000000 ) ;
#5046=CARTESIAN_POINT ( 'NONE',  ( -210.0000000000000000, 512.1906115401388888, -11.00000000000000000 ) ) ;
#5113=DIRECTION ( 'NONE',  ( -0.000000000000000000, -0.000000000000000000, 1.000000000000000000 ) ) ;
#5121=VECTOR ( 'NONE', #5168, 1000.000000000000000 ) ;
#5168=DIRECTION ( 'NONE',  ( 0.000000000000000000, -1.000000000000000000, 0.000000000000000000 ) ) ;
#5198=EDGE_CURVE ( 'NONE', #1964, #11502, #4363, .T. ) ;
#5235=EDGE_CURVE ( 'NONE', #9318, #414, #578, .T. ) ;
#5286=AXIS2_PLACEMENT_3D ( 'NONE', #13008, #1320, #4847 ) ;
#5367=AXIS2_PLACEMENT_3D ( 'NONE', #2643, #11575, #6322 ) ;
#5434=DIRECTION ( 'NONE',  ( -1.000000000000000000, 0.000000000000000000, 0.000000000000000000 ) ) ;
#5492=( NAMED_UNIT ( * ) PLANE_ANGLE_UNIT ( ) SI_UNIT ( $, .RADIAN. ) );
#5521=( NAMED_UNIT ( * ) SI_UNIT ( $, .STERADIAN. ) SOLID_ANGLE_UNIT ( ) );
#5533=LINE ( 'NONE', #10780, #14490 ) ;
#5567=LINE ( 'NONE', #9444, #7991 ) ;
#5579=DIRECTION ( 'NONE',  ( -0.000000000000000000, -0.000000000000000000, -1.000000000000000000 ) ) ;
#5591=COLOUR_RGB ( '', 0.31764706, 0.68627451, 0.89019608) ;
#5654=CARTESIAN_POINT ( 'NONE',  ( -430.0000000000000568, 425.7506394335853201, 109.9999999999999858 ) ) ;
#5752=CARTESIAN_POINT ( 'NONE',  ( 10.00000000000000000, 425.7506394335853201, 109.9999999999999858 ) ) ;
#5759=LINE ( 'NONE', #9812, #12469 ) ;
#5803=DIRECTION ( 'NONE',  ( 0.000000000000000000, 1.000000000000000000, 0.000000000000000000 ) ) ;
#5829=ADVANCED_FACE ( 'NONE', ( #6162 ), #15105, .F. ) ;
#5990=ORIENTED_EDGE ( 'NONE', *, *, #16207, .T. ) ;
#6024=ORIENTED_EDGE ( 'NONE', *, *, #6038, .T. ) ;
#6038=EDGE_CURVE ( 'NONE', #7123, #1069, #422, .T. ) ;
#6143=DIRECTION ( 'NONE',  ( -0.000000000000000000, -0.000000000000000000, 1.000000000000000000 ) ) ;
#6162=FACE_OUTER_BOUND ( 'NONE', #1473, .T. ) ;
#6191=VECTOR ( 'NONE', #332, 1000.000000000000000 ) ;
#6216=LINE ( 'NONE', #7418, #15111 ) ;
#6265=ORIENTED_EDGE ( 'NONE', *, *, #16426, .F. ) ;
#6267=LINE ( 'NONE', #2594, #12453 ) ;
#6272=CARTESIAN_POINT ( 'NONE',  ( -270.0000000000000000, 620.7506394335853201, -11.00000000000000000 ) ) ;
#6296=ORIENTED_EDGE ( 'NONE', *, *, #4256, .F. ) ;
#6322=DIRECTION ( 'NONE',  ( 0.000000000000000000, 0.000000000000000000, -1.000000000000000000 ) ) ;
#6445=DIRECTION ( 'NONE',  ( -0.000000000000000000, 0.000000000000000000, 1.000000000000000000 ) ) ;
#6453=ADVANCED_BREP_SHAPE_REPRESENTATION ( '', ( #3006, #1488 ), #13292 ) ;
#6482=LINE ( 'NONE', #16884, #7531 ) ;
#6487=EDGE_LOOP ( 'NONE', ( #8920, #12522, #13357, #1174 ) ) ;
#6599=SURFACE_STYLE_USAGE ( .BOTH. , #4222 ) ;
#6618=EDGE_LOOP ( 'NONE', ( #11767, #10206, #11073, #6296 ) ) ;
#6879=DIRECTION ( 'NONE',  ( 1.000000000000000000, 2.556703065963791256E-16, 0.000000000000000000 ) ) ;
#7021=ORIENTED_EDGE ( 'NONE', *, *, #194, .F. ) ;
#7035=CARTESIAN_POINT ( 'NONE',  ( -430.0000000000000568, 620.7506394335853201, 0.000000000000000000 ) ) ;
#7043=VECTOR ( 'NONE', #13094, 1000.000000000000000 ) ;
#7095=ORIENTED_EDGE ( 'NONE', *, *, #4037, .F. ) ;
#7123=VERTEX_POINT ( 'NONE', #12456 ) ;
#7133=ORIENTED_EDGE ( 'NONE', *, *, #16207, .F. ) ;
#7152=LINE ( 'NONE', #15329, #5121 ) ;
#7255=EDGE_CURVE ( 'NONE', #1496, #13088, #4959, .T. ) ;
#7261=ADVANCED_FACE ( 'NONE', ( #7877 ), #11753, .F. ) ;
#7280=CARTESIAN_POINT ( 'NONE',  ( -430.0000000000000568, 620.7506394335853201, 109.9999999999999858 ) ) ;
#7313=VERTEX_POINT ( 'NONE', #5654 ) ;
#7391=ORIENTED_EDGE ( 'NONE', *, *, #5235, .T. ) ;
#7418=CARTESIAN_POINT ( 'NONE',  ( 10.00000000000000000, 620.7506394335853201, 109.9999999999999858 ) ) ;
#7454=PRODUCT_CONTEXT ( 'NONE', #3036, 'mechanical' ) ;
#7531=VECTOR ( 'NONE', #11742, 1000.000000000000000 ) ;
#7655=LINE ( 'NONE', #15405, #13140 ) ;
#7675=CARTESIAN_POINT ( 'NONE',  ( -440.0000000000000568, 425.7506394335853201, -11.00000000000000000 ) ) ;
#7687=CIRCLE ( 'NONE', #14840, 60.00000000000002842 ) ;
#7702=EDGE_CURVE ( 'NONE', #13088, #414, #317, .T. ) ;
#7713=DIRECTION ( 'NONE',  ( 1.000000000000000000, -0.000000000000000000, -0.000000000000000000 ) ) ;
#7727=ORIENTED_EDGE ( 'NONE', *, *, #7255, .F. ) ;
#7730=DIRECTION ( 'NONE',  ( -1.000000000000000000, 0.000000000000000000, 0.000000000000000000 ) ) ;
#7748=CYLINDRICAL_SURFACE ( 'NONE', #9056, 60.00000000000002842 ) ;
#7755=ORIENTED_EDGE ( 'NONE', *, *, #11609, .T. ) ;
#7835=CARTESIAN_POINT ( 'NONE',  ( -440.0000000000000568, 620.7506394335853201, -11.00000000000000000 ) ) ;
#7837=CARTESIAN_POINT ( 'NONE',  ( -430.0000000000000568, 620.7506394335853201, 109.9999999999999858 ) ) ;
#7866=EDGE_CURVE ( 'NONE', #11485, #10332, #2012, .T. ) ;
#7877=FACE_OUTER_BOUND ( 'NONE', #1466, .T. ) ;
#7918=EDGE_CURVE ( 'NONE', #3171, #13742, #7152, .T. ) ;
#7991=VECTOR ( 'NONE', #10719, 1000.000000000000000 ) ;
#8016=ORIENTED_EDGE ( 'NONE', *, *, #12880, .F. ) ;
#8022=EDGE_CURVE ( 'NONE', #10332, #7313, #11374, .T. ) ;
#8125=EDGE_CURVE ( 'NONE', #7313, #8452, #2611, .T. ) ;
#8140=CARTESIAN_POINT ( 'NONE',  ( 10.00000000000000000, 425.7506394335853201, -11.00000000000000000 ) ) ;
#8225=CARTESIAN_POINT ( 'NONE',  ( -150.0000000000000000, 512.1906115401388888, -11.00000000000000000 ) ) ;
#8241=EDGE_CURVE ( 'NONE', #10036, #1964, #3444, .T. ) ;
#8252=( NAMED_UNIT ( * ) SI_UNIT ( $, .STERADIAN. ) SOLID_ANGLE_UNIT ( ) );
#8424=DIRECTION ( 'NONE',  ( 0.000000000000000000, -1.000000000000000000, -0.000000000000000000 ) ) ;
#8452=VERTEX_POINT ( 'NONE', #9095 ) ;
#8516=ORIENTED_EDGE ( 'NONE', *, *, #194, .T. ) ;
#8609=LINE ( 'NONE', #3123, #2301 ) ;
#8619=ORIENTED_EDGE ( 'NONE', *, *, #7702, .T. ) ;
#8654=PRODUCT_DEFINITION_CONTEXT ( 'detailed design', #1168, 'design' ) ;
#8657=EDGE_LOOP ( 'NONE', ( #8619, #15385, #9285, #10267 ) ) ;
#8664=CARTESIAN_POINT ( 'NONE',  ( -270.0000000000000000, 620.7506394335853201, -11.00000000000000000 ) ) ;
#8675=DIRECTION ( 'NONE',  ( 0.000000000000000000, 0.000000000000000000, -1.000000000000000000 ) ) ;
#8678=ADVANCED_FACE ( 'NONE', ( #13813 ), #16465, .F. ) ;
#8693=DIRECTION ( 'NONE',  ( 0.000000000000000000, 0.000000000000000000, 1.000000000000000000 ) ) ;
#8738=CARTESIAN_POINT ( 'NONE',  ( -270.0000000000000000, 620.7506394335853201, -11.00000000000000000 ) ) ;
#8755=DIRECTION ( 'NONE',  ( -1.000000000000000000, 0.000000000000000000, 0.000000000000000000 ) ) ;
#8764=CARTESIAN_POINT ( 'NONE',  ( 0.000000000000000000, 0.000000000000000000, 109.9999999999999858 ) ) ;
#8815=UNCERTAINTY_MEASURE_WITH_UNIT (LENGTH_MEASURE( 1.000000000000000082E-05 ), #13272, 'distance_accuracy_value', 'NONE');
#8880=MECHANICAL_DESIGN_GEOMETRIC_PRESENTATION_REPRESENTATION('',(#9433),#15725);
#8900=ORIENTED_EDGE ( 'NONE', *, *, #9740, .F. ) ;
#8920=ORIENTED_EDGE ( 'NONE', *, *, #4886, .F. ) ;
#8922=LINE ( 'NONE', #11743, #2237 ) ;
#8965=EDGE_CURVE ( 'NONE', #9650, #11502, #11378, .T. ) ;
#9051=FACE_OUTER_BOUND ( 'NONE', #4420, .T. ) ;
#9056=AXIS2_PLACEMENT_3D ( 'NONE', #10424, #9145, #3567 ) ;
#9065=CARTESIAN_POINT ( 'NONE',  ( -150.0000000000000000, 512.1906115401388888, -11.00000000000000000 ) ) ;
#9095=CARTESIAN_POINT ( 'NONE',  ( -430.0000000000000568, 620.7506394335853201, 109.9999999999999858 ) ) ;
#9145=DIRECTION ( 'NONE',  ( -0.000000000000000000, -0.000000000000000000, 1.000000000000000000 ) ) ;
#9195=ADVANCED_FACE ( 'NONE', ( #15507 ), #7748, .F. ) ;
#9196=VECTOR ( 'NONE', #12939, 1000.000000000000000 ) ;
#9285=ORIENTED_EDGE ( 'NONE', *, *, #13841, .F. ) ;
#9288=PRESENTATION_STYLE_ASSIGNMENT (( #6599 ) ) ;
#9318=VERTEX_POINT ( 'NONE', #10478 ) ;
#9328=CARTESIAN_POINT ( 'NONE',  ( 10.00000000000000000, 620.7506394335853201, -11.00000000000000000 ) ) ;
#9329=DIRECTION ( 'NONE',  ( -0.000000000000000000, -0.000000000000000000, 1.000000000000000000 ) ) ;
#9395=ORIENTED_EDGE ( 'NONE', *, *, #1342, .T. ) ;
#9433=STYLED_ITEM ( 'NONE', ( #9288 ), #3006 ) ;
#9444=CARTESIAN_POINT ( 'NONE',  ( 0.000000000000000000, 620.7506394335853201, 305.2562418976663707 ) ) ;
#9465=AXIS2_PLACEMENT_3D ( 'NONE', #15343, #3496, #13888 ) ;
#9526=CARTESIAN_POINT ( 'NONE',  ( 0.000000000000000000, 620.7506394335853201, 109.9999999999999858 ) ) ;
#9581=CARTESIAN_POINT ( 'NONE',  ( -150.0000000000000000, 512.1906115401388888, 0.000000000000000000 ) ) ;
#9634=EDGE_CURVE ( 'NONE', #15340, #9650, #7687, .T. ) ;
#9650=VERTEX_POINT ( 'NONE', #15941 ) ;
#9740=EDGE_CURVE ( 'NONE', #414, #7123, #6216, .T. ) ;
#9752=DIRECTION ( 'NONE',  ( -1.000000000000000000, 0.000000000000000000, 0.000000000000000000 ) ) ;
#9807=EDGE_LOOP ( 'NONE', ( #7021, #532, #16728, #12041 ) ) ;
#9812=CARTESIAN_POINT ( 'NONE',  ( -440.0000000000000568, 620.7506394335853201, -11.00000000000000000 ) ) ;
#9928=CARTESIAN_POINT ( 'NONE',  ( 10.00000000000000000, 620.7506394335853201, 0.000000000000000000 ) ) ;
#9933=DIRECTION ( 'NONE',  ( -1.000000000000000000, 0.000000000000000000, 0.000000000000000000 ) ) ;
#10036=VERTEX_POINT ( 'NONE', #15663 ) ;
#10087=LINE ( 'NONE', #16681, #4207 ) ;
#10206=ORIENTED_EDGE ( 'NONE', *, *, #7866, .F. ) ;
#10267=ORIENTED_EDGE ( 'NONE', *, *, #4064, .F. ) ;
#10332=VERTEX_POINT ( 'NONE', #14030 ) ;
#10352=ORIENTED_EDGE ( 'NONE', *, *, #1342, .F. ) ;
#10362=CARTESIAN_POINT ( 'NONE',  ( -150.0000000000000284, 620.7506394335853201, -11.00000000000000000 ) ) ;
#10379=LINE ( 'NONE', #15691, #2253 ) ;
#10424=CARTESIAN_POINT ( 'NONE',  ( -210.0000000000000000, 512.1906115401388888, -11.00000000000000000 ) ) ;
#10461=DIRECTION ( 'NONE',  ( 0.000000000000000000, 0.000000000000000000, 1.000000000000000000 ) ) ;
#10478=CARTESIAN_POINT ( 'NONE',  ( 10.00000000000000000, 425.7506394335853201, 109.9999999999999858 ) ) ;
#10597=FACE_OUTER_BOUND ( 'NONE', #12552, .T. ) ;
#10719=DIRECTION ( 'NONE',  ( -0.000000000000000000, -0.000000000000000000, -1.000000000000000000 ) ) ;
#10728=CARTESIAN_POINT ( 'NONE',  ( 0.000000000000000000, 425.7506394335853201, 305.2562418976663707 ) ) ;
#10741=ORIENTED_EDGE ( 'NONE', *, *, #10754, .F. ) ;
#10754=EDGE_CURVE ( 'NONE', #3722, #3171, #14346, .T. ) ;
#10780=CARTESIAN_POINT ( 'NONE',  ( -430.0000000000000568, 425.7506394335853201, 109.9999999999999858 ) ) ;
#10849=VECTOR ( 'NONE', #3405, 1000.000000000000000 ) ;
#10869=ADVANCED_FACE ( 'NONE', ( #12809 ), #16825, .F. ) ;
#10942=FACE_OUTER_BOUND ( 'NONE', #12912, .T. ) ;
#10943=ORIENTED_EDGE ( 'NONE', *, *, #11478, .F. ) ;
#10986=EDGE_CURVE ( 'NONE', #8452, #1964, #1965, .T. ) ;
#10994=DIRECTION ( 'NONE',  ( -0.000000000000000000, -0.000000000000000000, -1.000000000000000000 ) ) ;
#11020=ORIENTED_EDGE ( 'NONE', *, *, #8241, .T. ) ;
#11073=ORIENTED_EDGE ( 'NONE', *, *, #11609, .F. ) ;
#11086=CIRCLE ( 'NONE', #3681, 60.00000000000002842 ) ;
#11195=EDGE_LOOP ( 'NONE', ( #16072, #7391, #16126, #6024 ) ) ;
#11267=ORIENTED_EDGE ( 'NONE', *, *, #7918, .T. ) ;
#11273=EDGE_CURVE ( 'NONE', #11305, #3047, #10379, .T. ) ;
#11305=VERTEX_POINT ( 'NONE', #8140 ) ;
#11364=VECTOR ( 'NONE', #5579, 1000.000000000000000 ) ;
#11374=LINE ( 'NONE', #3896, #15830 ) ;
#11378=LINE ( 'NONE', #906, #1367 ) ;
#11380=ORIENTED_EDGE ( 'NONE', *, *, #5198, .F. ) ;
#11403=LINE ( 'NONE', #16640, #9196 ) ;
#11408=CARTESIAN_POINT ( 'NONE',  ( 0.000000000000000000, 425.7506394335853201, 0.000000000000000000 ) ) ;
#11422=CARTESIAN_POINT ( 'NONE',  ( -430.0000000000000568, 620.7506394335853201, 0.000000000000000000 ) ) ;
#11423=DIRECTION ( 'NONE',  ( -0.000000000000000000, 0.000000000000000000, 1.000000000000000000 ) ) ;
#11478=EDGE_CURVE ( 'NONE', #1496, #3722, #10087, .T. ) ;
#11485=VERTEX_POINT ( 'NONE', #12493 ) ;
#11502=VERTEX_POINT ( 'NONE', #13562 ) ;
#11575=DIRECTION ( 'NONE',  ( 0.000000000000000000, -1.000000000000000000, -0.000000000000000000 ) ) ;
#11609=EDGE_CURVE ( 'NONE', #2613, #11485, #2767, .T. ) ;
#11690=ORIENTED_EDGE ( 'NONE', *, *, #12548, .T. ) ;
#11702=FACE_OUTER_BOUND ( 'NONE', #8657, .T. ) ;
#11742=DIRECTION ( 'NONE',  ( -0.000000000000000000, -0.000000000000000000, 1.000000000000000000 ) ) ;
#11743=CARTESIAN_POINT ( 'NONE',  ( 10.00000000000000000, 425.7506394335853201, -11.00000000000000000 ) ) ;
#11753=PLANE ( 'NONE',  #5367 ) ;
#11767=ORIENTED_EDGE ( 'NONE', *, *, #12880, .T. ) ;
#11792=CARTESIAN_POINT ( 'NONE',  ( 10.00000000000000000, 620.7506394335853201, -11.00000000000000000 ) ) ;
#11880=ADVANCED_FACE ( 'NONE', ( #2948 ), #545, .F. ) ;
#11982=SHAPE_REPRESENTATION_RELATIONSHIP ( 'NONE' , 'NONE' ,  #16471, #6453 ) ;
#12019=ORIENTED_EDGE ( 'NONE', *, *, #1652, .F. ) ;
#12041=ORIENTED_EDGE ( 'NONE', *, *, #9634, .F. ) ;
#12097=ORIENTED_EDGE ( 'NONE', *, *, #7255, .T. ) ;
#12137=DIRECTION ( 'NONE',  ( -2.556703065963791256E-16, 1.000000000000000000, 0.000000000000000000 ) ) ;
#12145=LINE ( 'NONE', #11792, #4734 ) ;
#12154=ORIENTED_EDGE ( 'NONE', *, *, #4064, .T. ) ;
#12161=AXIS2_PLACEMENT_3D ( 'NONE', #4891, #15456, #9752 ) ;
#12437=CARTESIAN_POINT ( 'NONE',  ( 0.000000000000000000, 0.000000000000000000, 109.9999999999999858 ) ) ;
#12453=VECTOR ( 'NONE', #7730, 1000.000000000000000 ) ;
#12456=CARTESIAN_POINT ( 'NONE',  ( 0.000000000000000000, 620.7506394335853201, 109.9999999999999858 ) ) ;
#12469=VECTOR ( 'NONE', #2067, 1000.000000000000000 ) ;
#12493=CARTESIAN_POINT ( 'NONE',  ( -440.0000000000000568, 620.7506394335853201, 109.9999999999999858 ) ) ;
#12505=ORIENTED_EDGE ( 'NONE', *, *, #15868, .T. ) ;
#12522=ORIENTED_EDGE ( 'NONE', *, *, #15681, .F. ) ;
#12529=FACE_OUTER_BOUND ( 'NONE', #13277, .T. ) ;
#12548=EDGE_CURVE ( 'NONE', #14448, #1410, #11086, .T. ) ;
#12552=EDGE_LOOP ( 'NONE', ( #14519, #10741, #15581, #3741, #1999, #11380, #2853, #7095 ) ) ;
#12674=VECTOR ( 'NONE', #10994, 1000.000000000000000 ) ;
#12681=LINE ( 'NONE', #8738, #16273 ) ;
#12781=ORIENTED_EDGE ( 'NONE', *, *, #4791, .T. ) ;
#12783=VECTOR ( 'NONE', #1359, 1000.000000000000000 ) ;
#12809=FACE_OUTER_BOUND ( 'NONE', #6618, .T. ) ;
#12880=EDGE_CURVE ( 'NONE', #3047, #10332, #14058, .T. ) ;
#12906=CARTESIAN_POINT ( 'NONE',  ( -440.0000000000000568, 620.7506394335853201, -11.00000000000000000 ) ) ;
#12912=EDGE_LOOP ( 'NONE', ( #13055, #14533, #1816, #12781 ) ) ;
#12939=DIRECTION ( 'NONE',  ( -1.000000000000000000, -0.000000000000000000, -0.000000000000000000 ) ) ;
#12972=CARTESIAN_POINT ( 'NONE',  ( 10.00000000000000000, 620.7506394335853201, 0.000000000000000000 ) ) ;
#12997=PLANE ( 'NONE',  #14650 ) ;
#13008=CARTESIAN_POINT ( 'NONE',  ( 10.00000000000000000, 425.7506394335853201, -11.00000000000000000 ) ) ;
#13055=ORIENTED_EDGE ( 'NONE', *, *, #7866, .T. ) ;
#13088=VERTEX_POINT ( 'NONE', #9328 ) ;
#13094=DIRECTION ( 'NONE',  ( -0.000000000000000000, 1.000000000000000000, -0.000000000000000000 ) ) ;
#13140=VECTOR ( 'NONE', #4751, 1000.000000000000000 ) ;
#13241=SURFACE_STYLE_FILL_AREA ( #14705 ) ;
#13272=( LENGTH_UNIT ( ) NAMED_UNIT ( * ) SI_UNIT ( .MILLI., .METRE. ) );
#13277=EDGE_LOOP ( 'NONE', ( #15853, #9395, #11267, #7133 ) ) ;
#13292=( GEOMETRIC_REPRESENTATION_CONTEXT ( 3 ) GLOBAL_UNCERTAINTY_ASSIGNED_CONTEXT ( ( #8815 ) ) GLOBAL_UNIT_ASSIGNED_CONTEXT ( ( #13272, #14640, #5521 ) ) REPRESENTATION_CONTEXT ( 'NONE', 'WORKASPACE' ) );
#13357=ORIENTED_EDGE ( 'NONE', *, *, #16426, .T. ) ;
#13399=EDGE_CURVE ( 'NONE', #3722, #15340, #7655, .T. ) ;
#13428=CARTESIAN_POINT ( 'NONE',  ( 10.00000000000000000, 620.7506394335853201, -11.00000000000000000 ) ) ;
#13436=CARTESIAN_POINT ( 'NONE',  ( -150.0000000000000284, 620.7506394335853201, -11.00000000000000000 ) ) ;
#13562=CARTESIAN_POINT ( 'NONE',  ( -270.0000000000000000, 620.7506394335853201, 0.000000000000000000 ) ) ;
#13644=DIRECTION ( 'NONE',  ( -0.000000000000000000, -0.000000000000000000, -1.000000000000000000 ) ) ;
#13648=ORIENTED_EDGE ( 'NONE', *, *, #2049, .F. ) ;
#13685=VECTOR ( 'NONE', #527, 1000.000000000000000 ) ;
#13732=PLANE ( 'NONE',  #2514 ) ;
#13742=VERTEX_POINT ( 'NONE', #11408 ) ;
#13813=FACE_OUTER_BOUND ( 'NONE', #6487, .T. ) ;
#13841=EDGE_CURVE ( 'NONE', #11305, #9318, #8922, .T. ) ;
#13888=DIRECTION ( 'NONE',  ( 0.000000000000000000, 0.000000000000000000, 1.000000000000000000 ) ) ;
#13895=FACE_OUTER_BOUND ( 'NONE', #11195, .T. ) ;
#13896=DIRECTION ( 'NONE',  ( -0.000000000000000000, 0.000000000000000000, 1.000000000000000000 ) ) ;
#13974=ORIENTED_EDGE ( 'NONE', *, *, #10986, .T. ) ;
#14030=CARTESIAN_POINT ( 'NONE',  ( -440.0000000000000568, 425.7506394335853201, 109.9999999999999858 ) ) ;
#14058=LINE ( 'NONE', #7675, #561 ) ;
#14133=DIRECTION ( 'NONE',  ( 1.000000000000000000, 0.000000000000000000, 0.000000000000000000 ) ) ;
#14140=VECTOR ( 'NONE', #5803, 1000.000000000000000 ) ;
#14176=DIRECTION ( 'NONE',  ( 1.000000000000000000, 0.000000000000000000, 0.000000000000000000 ) ) ;
#14261=CARTESIAN_POINT ( 'NONE',  ( -440.0000000000000568, 620.7506394335853201, -11.00000000000000000 ) ) ;
#14288=PLANE ( 'NONE',  #5286 ) ;
#14346=LINE ( 'NONE', #12972, #16515 ) ;
#14448=VERTEX_POINT ( 'NONE', #1458 ) ;
#14464=DIRECTION ( 'NONE',  ( -0.000000000000000000, -0.000000000000000000, 1.000000000000000000 ) ) ;
#14490=VECTOR ( 'NONE', #4266, 1000.000000000000000 ) ;
#14515=DIRECTION ( 'NONE',  ( 0.000000000000000000, 0.000000000000000000, -1.000000000000000000 ) ) ;
#14519=ORIENTED_EDGE ( 'NONE', *, *, #7918, .F. ) ;
#14533=ORIENTED_EDGE ( 'NONE', *, *, #8022, .T. ) ;
#14640=( NAMED_UNIT ( * ) PLANE_ANGLE_UNIT ( ) SI_UNIT ( $, .RADIAN. ) );
#14650=AXIS2_PLACEMENT_3D ( 'NONE', #2421, #3807, #6445 ) ;
#14676=ADVANCED_FACE ( 'NONE', ( #12529 ), #16558, .F. ) ;
#14705=FILL_AREA_STYLE ('',( #1642 ) ) ;
#14727=DIRECTION ( 'NONE',  ( -0.000000000000000000, 0.000000000000000000, -1.000000000000000000 ) ) ;
#14764=ORIENTED_EDGE ( 'NONE', *, *, #4256, .T. ) ;
#14768=LINE ( 'NONE', #8225, #2780 ) ;
#14783=UNCERTAINTY_MEASURE_WITH_UNIT (LENGTH_MEASURE( 1.000000000000000082E-05 ), #16154, 'distance_accuracy_value', 'NONE');
#14840=AXIS2_PLACEMENT_3D ( 'NONE', #1788, #13644, #16124 ) ;
#14868=ORIENTED_EDGE ( 'NONE', *, *, #13841, .T. ) ;
#14872=DIRECTION ( 'NONE',  ( 0.000000000000000000, -1.000000000000000000, 0.000000000000000000 ) ) ;
#14938=VECTOR ( 'NONE', #14872, 1000.000000000000000 ) ;
#14939=DIRECTION ( 'NONE',  ( 1.000000000000000000, 0.000000000000000000, 0.000000000000000000 ) ) ;
#15105=PLANE ( 'NONE',  #3743 ) ;
#15108=LINE ( 'NONE', #5752, #13685 ) ;
#15111=VECTOR ( 'NONE', #9933, 1000.000000000000000 ) ;
#15131=ORIENTED_EDGE ( 'NONE', *, *, #11478, .T. ) ;
#15176=PLANE ( 'NONE',  #9465 ) ;
#15217=DIRECTION ( 'NONE',  ( 1.000000000000000000, 0.000000000000000000, 0.000000000000000000 ) ) ;
#15245=ORIENTED_EDGE ( 'NONE', *, *, #8022, .F. ) ;
#15278=DIRECTION ( 'NONE',  ( 1.000000000000000000, 0.000000000000000000, -0.000000000000000000 ) ) ;
#15329=CARTESIAN_POINT ( 'NONE',  ( 0.000000000000000000, 620.7506394335853201, 0.000000000000000000 ) ) ;
#15340=VERTEX_POINT ( 'NONE', #9581 ) ;
#15343=CARTESIAN_POINT ( 'NONE',  ( -430.0000000000000568, 620.7506394335853201, 109.9999999999999858 ) ) ;
#15385=ORIENTED_EDGE ( 'NONE', *, *, #5235, .F. ) ;
#15405=CARTESIAN_POINT ( 'NONE',  ( -149.9999999999998579, -3.835054598945682812E-14, 0.000000000000000000 ) ) ;
#15453=CARTESIAN_POINT ( 'NONE',  ( 10.00000000000000000, 620.7506394335853201, -11.00000000000000000 ) ) ;
#15456=DIRECTION ( 'NONE',  ( -0.000000000000000000, 0.000000000000000000, -1.000000000000000000 ) ) ;
#15507=FACE_OUTER_BOUND ( 'NONE', #9807, .T. ) ;
#15581=ORIENTED_EDGE ( 'NONE', *, *, #13399, .T. ) ;
#15657=ORIENTED_EDGE ( 'NONE', *, *, #8125, .F. ) ;
#15663=CARTESIAN_POINT ( 'NONE',  ( -430.0000000000000568, 425.7506394335853201, 0.000000000000000000 ) ) ;
#15681=EDGE_CURVE ( 'NONE', #16499, #14448, #3728, .T. ) ;
#15691=CARTESIAN_POINT ( 'NONE',  ( 10.00000000000000000, 425.7506394335853201, -11.00000000000000000 ) ) ;
#15695=ADVANCED_FACE ( 'NONE', ( #11702 ), #12997, .F. ) ;
#15725=( GEOMETRIC_REPRESENTATION_CONTEXT ( 3 ) GLOBAL_UNCERTAINTY_ASSIGNED_CONTEXT ( ( #14783 ) ) GLOBAL_UNIT_ASSIGNED_CONTEXT ( ( #16154, #5492, #8252 ) ) REPRESENTATION_CONTEXT ( 'NONE', 'WORKASPACE' ) );
#15830=VECTOR ( 'NONE', #14133, 1000.000000000000000 ) ;
#15853=ORIENTED_EDGE ( 'NONE', *, *, #6038, .F. ) ;
#15868=EDGE_CURVE ( 'NONE', #1410, #1496, #8609, .T. ) ;
#15941=CARTESIAN_POINT ( 'NONE',  ( -270.0000000000000000, 512.1906115401388888, 0.000000000000000000 ) ) ;
#15973=AXIS2_PLACEMENT_3D ( 'NONE', #4873, #15278, #2210 ) ;
#15992=VECTOR ( 'NONE', #14464, 1000.000000000000000 ) ;
#16072=ORIENTED_EDGE ( 'NONE', *, *, #2049, .T. ) ;
#16073=ORIENTED_EDGE ( 'NONE', *, *, #10986, .F. ) ;
#16090=CARTESIAN_POINT ( 'NONE',  ( 0.000000000000000000, 0.000000000000000000, 0.000000000000000000 ) ) ;
#16124=DIRECTION ( 'NONE',  ( -1.000000000000000000, 0.000000000000000000, 0.000000000000000000 ) ) ;
#16126=ORIENTED_EDGE ( 'NONE', *, *, #9740, .T. ) ;
#16154=( LENGTH_UNIT ( ) NAMED_UNIT ( * ) SI_UNIT ( .MILLI., .METRE. ) );
#16190=CARTESIAN_POINT ( 'NONE',  ( -440.0000000000000568, 620.7506394335853201, 109.9999999999999858 ) ) ;
#16201=PRODUCT_DEFINITION_SHAPE ( 'NONE', 'NONE',  #16487 ) ;
#16207=EDGE_CURVE ( 'NONE', #1069, #13742, #1291, .T. ) ;
#16273=VECTOR ( 'NONE', #6143, 1000.000000000000000 ) ;
#16328=ADVANCED_FACE ( 'NONE', ( #16627 ), #15176, .F. ) ;
#16340=ORIENTED_EDGE ( 'NONE', *, *, #15681, .T. ) ;
#16374=VECTOR ( 'NONE', #4432, 1000.000000000000000 ) ;
#16413=DIRECTION ( 'NONE',  ( -2.556703065963790763E-16, 1.000000000000000000, -0.000000000000000000 ) ) ;
#16426=EDGE_CURVE ( 'NONE', #16499, #11502, #12681, .T. ) ;
#16465=PLANE ( 'NONE',  #3512 ) ;
#16471=SHAPE_REPRESENTATION ( 'Part3', ( #1488 ), #13292 ) ;
#16487=PRODUCT_DEFINITION ( 'UNKNOWN', '', #1504, #8654 ) ;
#16496=CLOSED_SHELL ( 'NONE', ( #920, #7261, #15695, #898, #10869, #5829, #1023, #16328, #1109, #11880, #9195, #8678, #14676, #3425 ) ) ;
#16499=VERTEX_POINT ( 'NONE', #5022 ) ;
#16515=VECTOR ( 'NONE', #7713, 1000.000000000000000 ) ;
#16518=DIRECTION ( 'NONE',  ( -0.000000000000000000, -0.000000000000000000, 1.000000000000000000 ) ) ;
#16558=PLANE ( 'NONE',  #15973 ) ;
#16627=FACE_OUTER_BOUND ( 'NONE', #4946, .T. ) ;
#16640=CARTESIAN_POINT ( 'NONE',  ( -440.0000000000000568, 620.7506394335853201, 109.9999999999999858 ) ) ;
#16681=CARTESIAN_POINT ( 'NONE',  ( -150.0000000000000284, 620.7506394335853201, -11.00000000000000000 ) ) ;
#16728=ORIENTED_EDGE ( 'NONE', *, *, #4886, .T. ) ;
#16825=PLANE ( 'NONE',  #2803 ) ;
#16884=CARTESIAN_POINT ( 'NONE',  ( -270.0000000000000000, 512.1906115401388888, -11.00000000000000000 ) ) ;
ENDSEC;
END-ISO-10303-21;
